ISO-10303-21;
HEADER;
/* Generated by software containing ST-Developer
 * from STEP Tools, Inc. (www.steptools.com) 
 */

FILE_DESCRIPTION(
/* description */ ('Independent compact industrial fixture table, bolted aluminum worktop
 on connected adjustable support base. Whole-mm nominal dimensions. No
 load rating assigned.'),
/* implementation_level */ '2;1');

FILE_NAME(
/* name */ 'Flat washer M10.step',
/* time_stamp */ '2026-11-07T17:47:58-08:00',
/* author */ (''),
/* organization */ (''),
/* preprocessor_version */ 'ST-DEVELOPER v20.2',
/* originating_system */ 'Autodesk Translation Framework v15.17.0.0',
/* authorisation */ '');

FILE_SCHEMA (('AUTOMOTIVE_DESIGN { 1 0 10303 214 3 1 1 }'));
ENDSEC;

DATA;
#10=MECHANICAL_DESIGN_GEOMETRIC_PRESENTATION_REPRESENTATION('',(#2263),#97475);
#2225=SHAPE_REPRESENTATION_RELATIONSHIP('SRR','None',#97619,#2244);
#2244=ADVANCED_BREP_SHAPE_REPRESENTATION('',(#2282),#97469);
#2263=STYLED_ITEM('',(#97721),#2282);
#2282=MANIFOLD_SOLID_BREP('Body1',#21824);
#2357=FACE_BOUND('',#4475,.T.);
#2358=FACE_BOUND('',#4477,.T.);
#2505=PLANE('',#22988);
#2506=PLANE('',#22989);
#3249=FACE_OUTER_BOUND('',#4472,.T.);
#3250=FACE_OUTER_BOUND('',#4473,.T.);
#3251=FACE_OUTER_BOUND('',#4474,.T.);
#3252=FACE_OUTER_BOUND('',#4476,.T.);
#4472=EDGE_LOOP('',(#17154,#17155,#17156,#17157));
#4473=EDGE_LOOP('',(#17158,#17159,#17160,#17161));
#4474=EDGE_LOOP('',(#17162));
#4475=EDGE_LOOP('',(#17163));
#4476=EDGE_LOOP('',(#17164));
#4477=EDGE_LOOP('',(#17165));
#5724=LINE('',#70447,#6938);
#5725=LINE('',#70453,#6939);
#6938=VECTOR('',#26178,5.5);
#6939=VECTOR('',#26185,11.);
#7563=CIRCLE('',#22983,5.5);
#7564=CIRCLE('',#22984,5.5);
#7565=CIRCLE('',#22986,11.);
#7566=CIRCLE('',#22987,11.);
#8961=VERTEX_POINT('',#70444);
#8962=VERTEX_POINT('',#70446);
#8963=VERTEX_POINT('',#70450);
#8964=VERTEX_POINT('',#70452);
#11834=EDGE_CURVE('',#8961,#8961,#7563,.T.);
#11835=EDGE_CURVE('',#8961,#8962,#5724,.T.);
#11836=EDGE_CURVE('',#8962,#8962,#7564,.T.);
#11837=EDGE_CURVE('',#8963,#8963,#7565,.T.);
#11838=EDGE_CURVE('',#8963,#8964,#5725,.T.);
#11839=EDGE_CURVE('',#8964,#8964,#7566,.T.);
#17154=ORIENTED_EDGE('',*,*,#11834,.F.);
#17155=ORIENTED_EDGE('',*,*,#11835,.T.);
#17156=ORIENTED_EDGE('',*,*,#11836,.T.);
#17157=ORIENTED_EDGE('',*,*,#11835,.F.);
#17158=ORIENTED_EDGE('',*,*,#11837,.F.);
#17159=ORIENTED_EDGE('',*,*,#11838,.T.);
#17160=ORIENTED_EDGE('',*,*,#11839,.T.);
#17161=ORIENTED_EDGE('',*,*,#11838,.F.);
#17162=ORIENTED_EDGE('',*,*,#11837,.T.);
#17163=ORIENTED_EDGE('',*,*,#11834,.T.);
#17164=ORIENTED_EDGE('',*,*,#11839,.F.);
#17165=ORIENTED_EDGE('',*,*,#11836,.F.);
#20265=CYLINDRICAL_SURFACE('',#22982,5.5);
#20266=CYLINDRICAL_SURFACE('',#22985,11.);
#21369=ADVANCED_FACE('',(#3249),#20265,.F.);
#21370=ADVANCED_FACE('',(#3250),#20266,.T.);
#21371=ADVANCED_FACE('',(#3251,#2357),#2505,.T.);
#21372=ADVANCED_FACE('',(#3252,#2358),#2506,.F.);
#21824=CLOSED_SHELL('',(#21369,#21370,#21371,#21372));
#22981=AXIS2_PLACEMENT_3D('',#70442,#26172,#26173);
#22982=AXIS2_PLACEMENT_3D('',#70443,#26174,#26175);
#22983=AXIS2_PLACEMENT_3D('',#70445,#26176,#26177);
#22984=AXIS2_PLACEMENT_3D('',#70448,#26179,#26180);
#22985=AXIS2_PLACEMENT_3D('',#70449,#26181,#26182);
#22986=AXIS2_PLACEMENT_3D('',#70451,#26183,#26184);
#22987=AXIS2_PLACEMENT_3D('',#70454,#26186,#26187);
#22988=AXIS2_PLACEMENT_3D('',#70455,#26188,#26189);
#22989=AXIS2_PLACEMENT_3D('',#70456,#26190,#26191);
#26172=DIRECTION('axis',(0.,0.,1.));
#26173=DIRECTION('refdir',(1.,0.,0.));
#26174=DIRECTION('center_axis',(0.,0.,1.));
#26175=DIRECTION('ref_axis',(1.,0.,0.));
#26176=DIRECTION('center_axis',(0.,0.,-1.));
#26177=DIRECTION('ref_axis',(1.,0.,0.));
#26178=DIRECTION('',(0.,0.,-1.));
#26179=DIRECTION('center_axis',(0.,0.,-1.));
#26180=DIRECTION('ref_axis',(1.,0.,0.));
#26181=DIRECTION('center_axis',(0.,0.,1.));
#26182=DIRECTION('ref_axis',(1.,0.,0.));
#26183=DIRECTION('center_axis',(0.,0.,1.));
#26184=DIRECTION('ref_axis',(1.,0.,0.));
#26185=DIRECTION('',(0.,0.,-1.));
#26186=DIRECTION('center_axis',(0.,0.,1.));
#26187=DIRECTION('ref_axis',(1.,0.,0.));
#26188=DIRECTION('center_axis',(0.,0.,1.));
#26189=DIRECTION('ref_axis',(1.,0.,0.));
#26190=DIRECTION('center_axis',(0.,0.,1.));
#26191=DIRECTION('ref_axis',(1.,0.,0.));
#70442=CARTESIAN_POINT('',(0.,0.,0.));
#70443=CARTESIAN_POINT('Origin',(0.,0.,0.));
#70444=CARTESIAN_POINT('',(-5.5,-6.73555739531044E-16,2.));
#70445=CARTESIAN_POINT('Origin',(0.,0.,2.));
#70446=CARTESIAN_POINT('',(-5.5,-6.73555739531044E-16,0.));
#70447=CARTESIAN_POINT('',(-5.5,-6.73555739531044E-16,0.));
#70448=CARTESIAN_POINT('Origin',(0.,0.,0.));
#70449=CARTESIAN_POINT('Origin',(0.,0.,0.));
#70450=CARTESIAN_POINT('',(-11.,-1.34711147906209E-15,2.));
#70451=CARTESIAN_POINT('Origin',(0.,0.,2.));
#70452=CARTESIAN_POINT('',(-11.,-1.34711147906209E-15,0.));
#70453=CARTESIAN_POINT('',(-11.,-1.34711147906209E-15,0.));
#70454=CARTESIAN_POINT('Origin',(0.,0.,0.));
#70455=CARTESIAN_POINT('Origin',(0.,0.,2.));
#70456=CARTESIAN_POINT('Origin',(0.,0.,0.));
#97446=UNCERTAINTY_MEASURE_WITH_UNIT(LENGTH_MEASURE(0.01),#97476,
'DISTANCE_ACCURACY_VALUE',
'Maximum model space distance between geometric entities at asserted c
onnectivities');
#97452=UNCERTAINTY_MEASURE_WITH_UNIT(LENGTH_MEASURE(0.01),#97476,
'DISTANCE_ACCURACY_VALUE',
'Maximum model space distance between geometric entities at asserted c
onnectivities');
#97469=(
GEOMETRIC_REPRESENTATION_CONTEXT(3)
GLOBAL_UNCERTAINTY_ASSIGNED_CONTEXT((#97446))
GLOBAL_UNIT_ASSIGNED_CONTEXT((#97476,#97478,#97479))
REPRESENTATION_CONTEXT('','3D')
);
#97475=(
GEOMETRIC_REPRESENTATION_CONTEXT(3)
GLOBAL_UNCERTAINTY_ASSIGNED_CONTEXT((#97452))
GLOBAL_UNIT_ASSIGNED_CONTEXT((#97476,#97478,#97479))
REPRESENTATION_CONTEXT('','3D')
);
#97476=(
LENGTH_UNIT()
NAMED_UNIT(*)
SI_UNIT(.MILLI.,.METRE.)
);
#97478=(
NAMED_UNIT(*)
PLANE_ANGLE_UNIT()
SI_UNIT($,.RADIAN.)
);
#97479=(
NAMED_UNIT(*)
SI_UNIT($,.STERADIAN.)
SOLID_ANGLE_UNIT()
);
#97496=SHAPE_DEFINITION_REPRESENTATION(#97558,#97619);
#97558=PRODUCT_DEFINITION_SHAPE('',$,#97642);
#97619=SHAPE_REPRESENTATION('',(#22981),#97469);
#97625=PRODUCT_DEFINITION_CONTEXT('part definition',#97693,'design');
#97642=PRODUCT_DEFINITION('Flat washer M10','Flat washer M10',#97664,#97625);
#97664=PRODUCT_DEFINITION_FORMATION('',$,#97711);
#97693=APPLICATION_CONTEXT(
'Core Data for Automotive Mechanical Design Process');
#97694=PRODUCT_CONTEXT('part definition',#97693,'mechanical');
#97711=PRODUCT('Flat washer M10','Flat washer M10',$,(#97694));
#97721=PRESENTATION_STYLE_ASSIGNMENT((#97728));
#97728=SURFACE_STYLE_USAGE(.BOTH.,#97735);
#97735=SURFACE_SIDE_STYLE('',(#97742));
#97742=SURFACE_STYLE_FILL_AREA(#97749);
#97749=FILL_AREA_STYLE('Light gray',(#97756));
#97756=FILL_AREA_STYLE_COLOUR('Light gray',#97763);
#97763=COLOUR_RGB('Light gray',0.725490196078431,0.752941176470588,0.792156862745098);
ENDSEC;
END-ISO-10303-21;
